ISO-10303-21;
HEADER;
FILE_DESCRIPTION (('STEP AP214'),
    '1' );
FILE_NAME ('Base Mounting Plate.step',
    '2026-10-07T17:53:07',
    ( '' ),
    ( '' ),
    'SwSTEP 2.0',
    'SolidWorks 2025',
    '' );
FILE_SCHEMA (( 'AUTOMOTIVE_DESIGN' ));
ENDSEC;

DATA;
#34=ADVANCED_FACE ( 'NONE', ( #9475 ), #12553, .F. ) ;
#127=UNCERTAINTY_MEASURE_WITH_UNIT (LENGTH_MEASURE( 1.000000000000000082E-05 ), #7321, 'distance_accuracy_value', 'NONE');
#230=EDGE_CURVE ( 'NONE', #7248, #13568, #2901, .T. ) ;
#284=COLOUR_RGB ( '', 0.66274510, 0.83137255, 0.94901961) ;
#325=ORIENTED_EDGE ( 'NONE', *, *, #2125, .F. ) ;
#348=MANIFOLD_SOLID_BREP ( 'Boss-Extrude1', #11944 ) ;
#434=CARTESIAN_POINT ( 'NONE',  ( -27.49999999999998934, 0.000000000000000000, -30.00000000000000355 ) ) ;
#464=( GEOMETRIC_REPRESENTATION_CONTEXT ( 3 ) GLOBAL_UNCERTAINTY_ASSIGNED_CONTEXT ( ( #127 ) ) GLOBAL_UNIT_ASSIGNED_CONTEXT ( ( #7321, #10560, #2120 ) ) REPRESENTATION_CONTEXT ( 'NONE', 'WORKASPACE' ) );
#470=AXIS2_PLACEMENT_3D ( 'NONE', #9417, #10656, #8354 ) ;
#530=LINE ( 'NONE', #5893, #7154 ) ;
#630=AXIS2_PLACEMENT_3D ( 'NONE', #3794, #7899, #5933 ) ;
#887=LINE ( 'NONE', #3967, #2339 ) ;
#961=LINE ( 'NONE', #5143, #2985 ) ;
#970=ORIENTED_EDGE ( 'NONE', *, *, #2125, .T. ) ;
#990=PRESENTATION_STYLE_ASSIGNMENT (( #6217 ) ) ;
#1090=LINE ( 'NONE', #7486, #2247 ) ;
#1125=DIRECTION ( 'NONE',  ( -1.000000000000000000, 0.000000000000000000, 0.000000000000000000 ) ) ;
#1159=DIRECTION ( 'NONE',  ( 1.000000000000000000, 0.000000000000000000, 0.000000000000000000 ) ) ;
#1174=FACE_OUTER_BOUND ( 'NONE', #13468, .T. ) ;
#1270=VERTEX_POINT ( 'NONE', #10383 ) ;
#1383=DIRECTION ( 'NONE',  ( 0.000000000000000000, -0.000000000000000000, -1.000000000000000000 ) ) ;
#1395=VECTOR ( 'NONE', #3256, 1000.000000000000000 ) ;
#1428=CARTESIAN_POINT ( 'NONE',  ( -27.49999999999998934, 9.000000000000000000, 29.99999999999999645 ) ) ;
#1619=VECTOR ( 'NONE', #3466, 1000.000000000000000 ) ;
#1644=DIRECTION ( 'NONE',  ( -0.000000000000000000, -1.000000000000000000, -0.000000000000000000 ) ) ;
#1755=VECTOR ( 'NONE', #2060, 1000.000000000000000 ) ;
#1882=ORIENTED_EDGE ( 'NONE', *, *, #5382, .F. ) ;
#2036=VERTEX_POINT ( 'NONE', #12359 ) ;
#2060=DIRECTION ( 'NONE',  ( -0.000000000000000000, -0.000000000000000000, 1.000000000000000000 ) ) ;
#2120=( NAMED_UNIT ( * ) SI_UNIT ( $, .STERADIAN. ) SOLID_ANGLE_UNIT ( ) );
#2125=EDGE_CURVE ( 'NONE', #7771, #13568, #7363, .T. ) ;
#2247=VECTOR ( 'NONE', #1159, 1000.000000000000000 ) ;
#2252=CARTESIAN_POINT ( 'NONE',  ( 27.50000000000001066, 0.000000000000000000, 29.99999999999999645 ) ) ;
#2278=VECTOR ( 'NONE', #6055, 1000.000000000000000 ) ;
#2339=VECTOR ( 'NONE', #5975, 1000.000000000000000 ) ;
#2398=EDGE_CURVE ( 'NONE', #1270, #2036, #530, .T. ) ;
#2457=CARTESIAN_POINT ( 'NONE',  ( 0.000000000000000000, 9.000000000000000000, 0.000000000000000000 ) ) ;
#2521=ORIENTED_EDGE ( 'NONE', *, *, #5106, .F. ) ;
#2764=LINE ( 'NONE', #434, #13713 ) ;
#2892=EDGE_CURVE ( 'NONE', #1270, #8617, #12251, .T. ) ;
#2901=LINE ( 'NONE', #7698, #1619 ) ;
#2985=VECTOR ( 'NONE', #4317, 1000.000000000000000 ) ;
#2990=ORIENTED_EDGE ( 'NONE', *, *, #9369, .T. ) ;
#3004=CARTESIAN_POINT ( 'NONE',  ( -27.49999999999998934, 9.000000000000000000, -30.00000000000000355 ) ) ;
#3042=DIRECTION ( 'NONE',  ( 0.000000000000000000, 0.000000000000000000, -1.000000000000000000 ) ) ;
#3069=PLANE ( 'NONE',  #470 ) ;
#3075=CARTESIAN_POINT ( 'NONE',  ( -27.49999999999998934, 0.000000000000000000, 29.99999999999999645 ) ) ;
#3176=SURFACE_STYLE_FILL_AREA ( #10414 ) ;
#3222=ORIENTED_EDGE ( 'NONE', *, *, #2398, .F. ) ;
#3256=DIRECTION ( 'NONE',  ( 0.000000000000000000, 0.000000000000000000, -1.000000000000000000 ) ) ;
#3318=VECTOR ( 'NONE', #7407, 1000.000000000000000 ) ;
#3434=AXIS2_PLACEMENT_3D ( 'NONE', #12906, #10421, #3042 ) ;
#3449=PLANE ( 'NONE',  #7908 ) ;
#3466=DIRECTION ( 'NONE',  ( -0.000000000000000000, -1.000000000000000000, -0.000000000000000000 ) ) ;
#3479=SHAPE_REPRESENTATION_RELATIONSHIP ( 'NONE' , 'NONE' ,  #11399, #6247 ) ;
#3561=DIRECTION ( 'NONE',  ( 0.000000000000000000, 0.000000000000000000, -1.000000000000000000 ) ) ;
#3748=( NAMED_UNIT ( * ) SI_UNIT ( $, .STERADIAN. ) SOLID_ANGLE_UNIT ( ) );
#3749=ADVANCED_FACE ( 'NONE', ( #5560 ), #11998, .F. ) ;
#3794=CARTESIAN_POINT ( 'NONE',  ( 0.000000000000000000, 0.000000000000000000, 0.000000000000000000 ) ) ;
#3967=CARTESIAN_POINT ( 'NONE',  ( -27.49999999999998934, 9.000000000000000000, -30.00000000000000355 ) ) ;
#4003=SURFACE_SIDE_STYLE ('',( #3176 ) ) ;
#4014=ADVANCED_FACE ( 'NONE', ( #6390 ), #3069, .F. ) ;
#4317=DIRECTION ( 'NONE',  ( -0.000000000000000000, -1.000000000000000000, -0.000000000000000000 ) ) ;
#4384=ORIENTED_EDGE ( 'NONE', *, *, #6022, .F. ) ;
#4411=PRODUCT_DEFINITION_SHAPE ( 'NONE', 'NONE',  #12939 ) ;
#4457=VECTOR ( 'NONE', #11007, 1000.000000000000000 ) ;
#4460=ORIENTED_EDGE ( 'NONE', *, *, #2892, .T. ) ;
#4469=PLANE ( 'NONE',  #3434 ) ;
#4559=DIRECTION ( 'NONE',  ( 0.000000000000000000, 0.000000000000000000, 1.000000000000000000 ) ) ;
#4570=CARTESIAN_POINT ( 'NONE',  ( -27.49999999999998934, 9.000000000000000000, 29.99999999999999645 ) ) ;
#4698=CARTESIAN_POINT ( 'NONE',  ( 27.50000000000001066, 9.000000000000000000, 29.99999999999999645 ) ) ;
#4761=APPLICATION_CONTEXT ( 'automotive_design' ) ;
#4835=PLANE ( 'NONE',  #630 ) ;
#4910=FACE_OUTER_BOUND ( 'NONE', #11526, .T. ) ;
#4930=PRODUCT_CONTEXT ( 'NONE', #13135, 'mechanical' ) ;
#4988=ORIENTED_EDGE ( 'NONE', *, *, #5382, .T. ) ;
#5012=PRODUCT_DEFINITION_CONTEXT ( 'detailed design', #4761, 'design' ) ;
#5106=EDGE_CURVE ( 'NONE', #6726, #6571, #961, .T. ) ;
#5126=LINE ( 'NONE', #11483, #1395 ) ;
#5143=CARTESIAN_POINT ( 'NONE',  ( 27.50000000000001066, 9.000000000000000000, -30.00000000000000355 ) ) ;
#5382=EDGE_CURVE ( 'NONE', #7248, #6726, #5126, .T. ) ;
#5482=ORIENTED_EDGE ( 'NONE', *, *, #6022, .T. ) ;
#5560=FACE_OUTER_BOUND ( 'NONE', #7527, .T. ) ;
#5687=ADVANCED_FACE ( 'NONE', ( #1174 ), #4469, .F. ) ;
#5756=( LENGTH_UNIT ( ) NAMED_UNIT ( * ) SI_UNIT ( .MILLI., .METRE. ) );
#5767=LINE ( 'NONE', #12143, #13099 ) ;
#5893=CARTESIAN_POINT ( 'NONE',  ( -27.49999999999998934, 9.000000000000000000, -30.00000000000000355 ) ) ;
#5933=DIRECTION ( 'NONE',  ( 0.000000000000000000, -0.000000000000000000, -1.000000000000000000 ) ) ;
#5975=DIRECTION ( 'NONE',  ( -1.000000000000000000, -0.000000000000000000, -0.000000000000000000 ) ) ;
#6022=EDGE_CURVE ( 'NONE', #6726, #1270, #887, .T. ) ;
#6055=DIRECTION ( 'NONE',  ( 1.000000000000000000, 0.000000000000000000, 0.000000000000000000 ) ) ;
#6217=SURFACE_STYLE_USAGE ( .BOTH. , #4003 ) ;
#6223=EDGE_CURVE ( 'NONE', #8617, #7248, #1090, .T. ) ;
#6225=( GEOMETRIC_REPRESENTATION_CONTEXT ( 3 ) GLOBAL_UNCERTAINTY_ASSIGNED_CONTEXT ( ( #12421 ) ) GLOBAL_UNIT_ASSIGNED_CONTEXT ( ( #5756, #13034, #3748 ) ) REPRESENTATION_CONTEXT ( 'NONE', 'WORKASPACE' ) );
#6247=ADVANCED_BREP_SHAPE_REPRESENTATION ( '', ( #348, #6434 ), #6225 ) ;
#6390=FACE_OUTER_BOUND ( 'NONE', #9785, .T. ) ;
#6434=AXIS2_PLACEMENT_3D ( 'NONE', #11654, #12825, #11856 ) ;
#6571=VERTEX_POINT ( 'NONE', #9196 ) ;
#6684=DIRECTION ( 'NONE',  ( 0.000000000000000000, -1.000000000000000000, 0.000000000000000000 ) ) ;
#6726=VERTEX_POINT ( 'NONE', #12044 ) ;
#7154=VECTOR ( 'NONE', #1644, 1000.000000000000000 ) ;
#7205=ORIENTED_EDGE ( 'NONE', *, *, #11671, .T. ) ;
#7218=DIRECTION ( 'NONE',  ( 1.000000000000000000, 0.000000000000000000, -0.000000000000000000 ) ) ;
#7248=VERTEX_POINT ( 'NONE', #4698 ) ;
#7321=( LENGTH_UNIT ( ) NAMED_UNIT ( * ) SI_UNIT ( .MILLI., .METRE. ) );
#7363=LINE ( 'NONE', #3075, #2278 ) ;
#7407=DIRECTION ( 'NONE',  ( -0.000000000000000000, -1.000000000000000000, -0.000000000000000000 ) ) ;
#7486=CARTESIAN_POINT ( 'NONE',  ( -27.49999999999998934, 9.000000000000000000, 29.99999999999999645 ) ) ;
#7527=EDGE_LOOP ( 'NONE', ( #4988, #5482, #4460, #10028 ) ) ;
#7529=ADVANCED_FACE ( 'NONE', ( #10706 ), #3449, .F. ) ;
#7536=ORIENTED_EDGE ( 'NONE', *, *, #230, .T. ) ;
#7574=ORIENTED_EDGE ( 'NONE', *, *, #6223, .F. ) ;
#7629=EDGE_CURVE ( 'NONE', #6571, #2036, #2764, .T. ) ;
#7698=CARTESIAN_POINT ( 'NONE',  ( 27.50000000000001066, 9.000000000000000000, 29.99999999999999645 ) ) ;
#7771=VERTEX_POINT ( 'NONE', #10068 ) ;
#7809=ORIENTED_EDGE ( 'NONE', *, *, #10046, .T. ) ;
#7899=DIRECTION ( 'NONE',  ( 0.000000000000000000, -1.000000000000000000, 0.000000000000000000 ) ) ;
#7908=AXIS2_PLACEMENT_3D ( 'NONE', #12856, #1125, #4559 ) ;
#8175=ORIENTED_EDGE ( 'NONE', *, *, #11671, .F. ) ;
#8212=DIRECTION ( 'NONE',  ( 0.000000000000000000, 0.000000000000000000, 1.000000000000000000 ) ) ;
#8354=DIRECTION ( 'NONE',  ( -1.000000000000000000, 0.000000000000000000, -0.000000000000000000 ) ) ;
#8411=AXIS2_PLACEMENT_3D ( 'NONE', #3004, #8212, #7218 ) ;
#8455=LINE ( 'NONE', #13556, #1755 ) ;
#8617=VERTEX_POINT ( 'NONE', #1428 ) ;
#9081=ORIENTED_EDGE ( 'NONE', *, *, #2892, .F. ) ;
#9165=DIRECTION ( 'NONE',  ( -1.000000000000000000, -0.000000000000000000, -0.000000000000000000 ) ) ;
#9196=CARTESIAN_POINT ( 'NONE',  ( 27.50000000000001066, 0.000000000000000000, -30.00000000000000355 ) ) ;
#9212=STYLED_ITEM ( 'NONE', ( #990 ), #348 ) ;
#9219=EDGE_LOOP ( 'NONE', ( #2990, #2521, #1882, #7536 ) ) ;
#9223=EDGE_LOOP ( 'NONE', ( #12663, #3222, #4384, #11885 ) ) ;
#9369=EDGE_CURVE ( 'NONE', #13568, #6571, #5767, .T. ) ;
#9417=CARTESIAN_POINT ( 'NONE',  ( -27.49999999999998934, 9.000000000000000000, 29.99999999999999645 ) ) ;
#9475=FACE_OUTER_BOUND ( 'NONE', #9223, .T. ) ;
#9660=PRODUCT ( 'Base Mounting Plate', 'Base Mounting Plate', '', ( #4930 ) ) ;
#9731=LINE ( 'NONE', #13768, #3318 ) ;
#9785=EDGE_LOOP ( 'NONE', ( #970, #10533, #7574, #7809 ) ) ;
#10010=ORIENTED_EDGE ( 'NONE', *, *, #9369, .F. ) ;
#10028=ORIENTED_EDGE ( 'NONE', *, *, #6223, .T. ) ;
#10046=EDGE_CURVE ( 'NONE', #8617, #7771, #9731, .T. ) ;
#10068=CARTESIAN_POINT ( 'NONE',  ( -27.49999999999998934, 0.000000000000000000, 29.99999999999999645 ) ) ;
#10383=CARTESIAN_POINT ( 'NONE',  ( -27.49999999999998934, 9.000000000000000000, -30.00000000000000355 ) ) ;
#10414=FILL_AREA_STYLE ('',( #12652 ) ) ;
#10421=DIRECTION ( 'NONE',  ( 1.000000000000000000, -0.000000000000000000, 0.000000000000000000 ) ) ;
#10494=AXIS2_PLACEMENT_3D ( 'NONE', #2457, #6684, #1383 ) ;
#10533=ORIENTED_EDGE ( 'NONE', *, *, #230, .F. ) ;
#10560=( NAMED_UNIT ( * ) PLANE_ANGLE_UNIT ( ) SI_UNIT ( $, .RADIAN. ) );
#10656=DIRECTION ( 'NONE',  ( 0.000000000000000000, 0.000000000000000000, -1.000000000000000000 ) ) ;
#10706=FACE_OUTER_BOUND ( 'NONE', #9219, .T. ) ;
#10835=MECHANICAL_DESIGN_GEOMETRIC_PRESENTATION_REPRESENTATION('',(#9212),#464);
#10942=ORIENTED_EDGE ( 'NONE', *, *, #10046, .F. ) ;
#11007=DIRECTION ( 'NONE',  ( -0.000000000000000000, -0.000000000000000000, 1.000000000000000000 ) ) ;
#11399=SHAPE_REPRESENTATION ( 'Base Mounting Plate', ( #6434 ), #6225 ) ;
#11483=CARTESIAN_POINT ( 'NONE',  ( 27.50000000000001066, 9.000000000000000000, 29.99999999999999645 ) ) ;
#11523=ADVANCED_FACE ( 'NONE', ( #4910 ), #4835, .T. ) ;
#11526=EDGE_LOOP ( 'NONE', ( #10010, #325, #8175, #13500 ) ) ;
#11654=CARTESIAN_POINT ( 'NONE',  ( 0.000000000000000000, 0.000000000000000000, 0.000000000000000000 ) ) ;
#11671=EDGE_CURVE ( 'NONE', #2036, #7771, #8455, .T. ) ;
#11856=DIRECTION ( 'NONE',  ( 1.000000000000000000, 0.000000000000000000, 0.000000000000000000 ) ) ;
#11885=ORIENTED_EDGE ( 'NONE', *, *, #5106, .T. ) ;
#11944=CLOSED_SHELL ( 'NONE', ( #7529, #34, #5687, #4014, #3749, #11523 ) ) ;
#11998=PLANE ( 'NONE',  #10494 ) ;
#12044=CARTESIAN_POINT ( 'NONE',  ( 27.50000000000001066, 9.000000000000000000, -30.00000000000000355 ) ) ;
#12143=CARTESIAN_POINT ( 'NONE',  ( 27.50000000000001066, 0.000000000000000000, 29.99999999999999645 ) ) ;
#12251=LINE ( 'NONE', #4570, #4457 ) ;
#12359=CARTESIAN_POINT ( 'NONE',  ( -27.49999999999998934, 0.000000000000000000, -30.00000000000000355 ) ) ;
#12421=UNCERTAINTY_MEASURE_WITH_UNIT (LENGTH_MEASURE( 1.000000000000000082E-05 ), #5756, 'distance_accuracy_value', 'NONE');
#12553=PLANE ( 'NONE',  #8411 ) ;
#12652=FILL_AREA_STYLE_COLOUR ( '', #284 ) ;
#12663=ORIENTED_EDGE ( 'NONE', *, *, #7629, .T. ) ;
#12698=PRODUCT_DEFINITION_FORMATION_WITH_SPECIFIED_SOURCE ( 'ANY', '', #9660, .NOT_KNOWN. ) ;
#12825=DIRECTION ( 'NONE',  ( 0.000000000000000000, 0.000000000000000000, 1.000000000000000000 ) ) ;
#12854=ORIENTED_EDGE ( 'NONE', *, *, #2398, .T. ) ;
#12856=CARTESIAN_POINT ( 'NONE',  ( 27.50000000000001066, 9.000000000000000000, 29.99999999999999645 ) ) ;
#12906=CARTESIAN_POINT ( 'NONE',  ( -27.49999999999998934, 9.000000000000000000, 29.99999999999999645 ) ) ;
#12939=PRODUCT_DEFINITION ( 'UNKNOWN', '', #12698, #5012 ) ;
#13034=( NAMED_UNIT ( * ) PLANE_ANGLE_UNIT ( ) SI_UNIT ( $, .RADIAN. ) );
#13099=VECTOR ( 'NONE', #3561, 1000.000000000000000 ) ;
#13135=APPLICATION_CONTEXT ( 'automotive_design' ) ;
#13468=EDGE_LOOP ( 'NONE', ( #7205, #10942, #9081, #12854 ) ) ;
#13500=ORIENTED_EDGE ( 'NONE', *, *, #7629, .F. ) ;
#13556=CARTESIAN_POINT ( 'NONE',  ( -27.49999999999998934, 0.000000000000000000, 29.99999999999999645 ) ) ;
#13568=VERTEX_POINT ( 'NONE', #2252 ) ;
#13654=SHAPE_DEFINITION_REPRESENTATION ( #4411, #11399 ) ;
#13713=VECTOR ( 'NONE', #9165, 1000.000000000000000 ) ;
#13768=CARTESIAN_POINT ( 'NONE',  ( -27.49999999999998934, 9.000000000000000000, 29.99999999999999645 ) ) ;
ENDSEC;
END-ISO-10303-21;
